ISO-10303-21;
HEADER;
/* Generated by software containing ST-Developer
 * from STEP Tools, Inc. (www.steptools.com) 
 */

FILE_DESCRIPTION(
/* description */ ('PAT-072'),
/* implementation_level */ '2;1');

FILE_NAME(
/* name */ 'Base.step',
/* time_stamp */ '2026-10-29T20:11:56-07:00',
/* author */ (''),
/* organization */ (''),
/* preprocessor_version */ 'ST-DEVELOPER v20.2',
/* originating_system */ 'Autodesk Translation Framework v15.17.0.0',
/* authorisation */ '');

FILE_SCHEMA (('AUTOMOTIVE_DESIGN { 1 0 10303 214 3 1 1 }'));
ENDSEC;

DATA;
#10=MECHANICAL_DESIGN_GEOMETRIC_PRESENTATION_REPRESENTATION('',(#332),#11432);
#260=SHAPE_REPRESENTATION_RELATIONSHIP('SRR','None',#11564,#296);
#296=ADVANCED_BREP_SHAPE_REPRESENTATION('',(#368),#11395);
#332=STYLED_ITEM('',(#11798),#368);
#368=MANIFOLD_SOLID_BREP('Body1',#6067);
#402=FACE_BOUND('',#1177,.T.);
#403=FACE_BOUND('',#1178,.T.);
#404=FACE_BOUND('',#1179,.T.);
#405=FACE_BOUND('',#1180,.T.);
#406=FACE_BOUND('',#1182,.T.);
#407=FACE_BOUND('',#1183,.T.);
#408=FACE_BOUND('',#1184,.T.);
#409=FACE_BOUND('',#1185,.T.);
#570=PLANE('',#6516);
#571=PLANE('',#6517);
#572=PLANE('',#6518);
#573=PLANE('',#6519);
#574=PLANE('',#6520);
#575=PLANE('',#6521);
#796=FACE_OUTER_BOUND('',#1168,.T.);
#797=FACE_OUTER_BOUND('',#1169,.T.);
#798=FACE_OUTER_BOUND('',#1170,.T.);
#799=FACE_OUTER_BOUND('',#1171,.T.);
#800=FACE_OUTER_BOUND('',#1172,.T.);
#801=FACE_OUTER_BOUND('',#1173,.T.);
#802=FACE_OUTER_BOUND('',#1174,.T.);
#803=FACE_OUTER_BOUND('',#1175,.T.);
#804=FACE_OUTER_BOUND('',#1176,.T.);
#805=FACE_OUTER_BOUND('',#1181,.T.);
#1168=EDGE_LOOP('',(#4068,#4069,#4070,#4071));
#1169=EDGE_LOOP('',(#4072,#4073,#4074,#4075));
#1170=EDGE_LOOP('',(#4076,#4077,#4078,#4079));
#1171=EDGE_LOOP('',(#4080,#4081,#4082,#4083));
#1172=EDGE_LOOP('',(#4084,#4085,#4086,#4087));
#1173=EDGE_LOOP('',(#4088,#4089,#4090,#4091));
#1174=EDGE_LOOP('',(#4092,#4093,#4094,#4095));
#1175=EDGE_LOOP('',(#4096,#4097,#4098,#4099));
#1176=EDGE_LOOP('',(#4100,#4101,#4102,#4103));
#1177=EDGE_LOOP('',(#4104));
#1178=EDGE_LOOP('',(#4105));
#1179=EDGE_LOOP('',(#4106));
#1180=EDGE_LOOP('',(#4107));
#1181=EDGE_LOOP('',(#4108,#4109,#4110,#4111));
#1182=EDGE_LOOP('',(#4112));
#1183=EDGE_LOOP('',(#4113));
#1184=EDGE_LOOP('',(#4114));
#1185=EDGE_LOOP('',(#4115));
#1708=LINE('',#9198,#2127);
#1709=LINE('',#9204,#2128);
#1710=LINE('',#9210,#2129);
#1711=LINE('',#9216,#2130);
#1712=LINE('',#9221,#2131);
#1713=LINE('',#9223,#2132);
#1714=LINE('',#9225,#2133);
#1715=LINE('',#9226,#2134);
#1716=LINE('',#9229,#2135);
#1717=LINE('',#9231,#2136);
#1718=LINE('',#9232,#2137);
#1719=LINE('',#9235,#2138);
#1720=LINE('',#9237,#2139);
#1721=LINE('',#9238,#2140);
#1722=LINE('',#9240,#2141);
#1723=LINE('',#9241,#2142);
#2127=VECTOR('',#7267,0.21);
#2128=VECTOR('',#7274,0.21);
#2129=VECTOR('',#7281,0.21);
#2130=VECTOR('',#7288,0.21);
#2131=VECTOR('',#7293,1.);
#2132=VECTOR('',#7294,1.);
#2133=VECTOR('',#7295,1.);
#2134=VECTOR('',#7296,1.);
#2135=VECTOR('',#7299,1.);
#2136=VECTOR('',#7300,1.);
#2137=VECTOR('',#7301,1.);
#2138=VECTOR('',#7304,1.);
#2139=VECTOR('',#7305,1.);
#2140=VECTOR('',#7306,1.);
#2141=VECTOR('',#7309,1.);
#2142=VECTOR('',#7310,1.);
#2546=CIRCLE('',#6505,0.21);
#2547=CIRCLE('',#6506,0.21);
#2548=CIRCLE('',#6508,0.21);
#2549=CIRCLE('',#6509,0.21);
#2550=CIRCLE('',#6511,0.21);
#2551=CIRCLE('',#6512,0.21);
#2552=CIRCLE('',#6514,0.21);
#2553=CIRCLE('',#6515,0.21);
#2836=VERTEX_POINT('',#9195);
#2837=VERTEX_POINT('',#9197);
#2838=VERTEX_POINT('',#9201);
#2839=VERTEX_POINT('',#9203);
#2840=VERTEX_POINT('',#9207);
#2841=VERTEX_POINT('',#9209);
#2842=VERTEX_POINT('',#9213);
#2843=VERTEX_POINT('',#9215);
#2844=VERTEX_POINT('',#9219);
#2845=VERTEX_POINT('',#9220);
#2846=VERTEX_POINT('',#9222);
#2847=VERTEX_POINT('',#9224);
#2848=VERTEX_POINT('',#9228);
#2849=VERTEX_POINT('',#9230);
#2850=VERTEX_POINT('',#9234);
#2851=VERTEX_POINT('',#9236);
#3323=EDGE_CURVE('',#2836,#2836,#2546,.T.);
#3324=EDGE_CURVE('',#2836,#2837,#1708,.T.);
#3325=EDGE_CURVE('',#2837,#2837,#2547,.T.);
#3326=EDGE_CURVE('',#2838,#2838,#2548,.T.);
#3327=EDGE_CURVE('',#2838,#2839,#1709,.T.);
#3328=EDGE_CURVE('',#2839,#2839,#2549,.T.);
#3329=EDGE_CURVE('',#2840,#2840,#2550,.T.);
#3330=EDGE_CURVE('',#2840,#2841,#1710,.T.);
#3331=EDGE_CURVE('',#2841,#2841,#2551,.T.);
#3332=EDGE_CURVE('',#2842,#2842,#2552,.T.);
#3333=EDGE_CURVE('',#2842,#2843,#1711,.T.);
#3334=EDGE_CURVE('',#2843,#2843,#2553,.T.);
#3335=EDGE_CURVE('',#2844,#2845,#1712,.T.);
#3336=EDGE_CURVE('',#2845,#2846,#1713,.T.);
#3337=EDGE_CURVE('',#2847,#2846,#1714,.T.);
#3338=EDGE_CURVE('',#2844,#2847,#1715,.T.);
#3339=EDGE_CURVE('',#2848,#2844,#1716,.T.);
#3340=EDGE_CURVE('',#2849,#2847,#1717,.T.);
#3341=EDGE_CURVE('',#2848,#2849,#1718,.T.);
#3342=EDGE_CURVE('',#2850,#2848,#1719,.T.);
#3343=EDGE_CURVE('',#2851,#2849,#1720,.T.);
#3344=EDGE_CURVE('',#2850,#2851,#1721,.T.);
#3345=EDGE_CURVE('',#2845,#2850,#1722,.T.);
#3346=EDGE_CURVE('',#2846,#2851,#1723,.T.);
#4068=ORIENTED_EDGE('',*,*,#3323,.F.);
#4069=ORIENTED_EDGE('',*,*,#3324,.T.);
#4070=ORIENTED_EDGE('',*,*,#3325,.F.);
#4071=ORIENTED_EDGE('',*,*,#3324,.F.);
#4072=ORIENTED_EDGE('',*,*,#3326,.F.);
#4073=ORIENTED_EDGE('',*,*,#3327,.T.);
#4074=ORIENTED_EDGE('',*,*,#3328,.F.);
#4075=ORIENTED_EDGE('',*,*,#3327,.F.);
#4076=ORIENTED_EDGE('',*,*,#3329,.F.);
#4077=ORIENTED_EDGE('',*,*,#3330,.T.);
#4078=ORIENTED_EDGE('',*,*,#3331,.F.);
#4079=ORIENTED_EDGE('',*,*,#3330,.F.);
#4080=ORIENTED_EDGE('',*,*,#3332,.F.);
#4081=ORIENTED_EDGE('',*,*,#3333,.T.);
#4082=ORIENTED_EDGE('',*,*,#3334,.F.);
#4083=ORIENTED_EDGE('',*,*,#3333,.F.);
#4084=ORIENTED_EDGE('',*,*,#3335,.T.);
#4085=ORIENTED_EDGE('',*,*,#3336,.T.);
#4086=ORIENTED_EDGE('',*,*,#3337,.F.);
#4087=ORIENTED_EDGE('',*,*,#3338,.F.);
#4088=ORIENTED_EDGE('',*,*,#3339,.T.);
#4089=ORIENTED_EDGE('',*,*,#3338,.T.);
#4090=ORIENTED_EDGE('',*,*,#3340,.F.);
#4091=ORIENTED_EDGE('',*,*,#3341,.F.);
#4092=ORIENTED_EDGE('',*,*,#3342,.T.);
#4093=ORIENTED_EDGE('',*,*,#3341,.T.);
#4094=ORIENTED_EDGE('',*,*,#3343,.F.);
#4095=ORIENTED_EDGE('',*,*,#3344,.F.);
#4096=ORIENTED_EDGE('',*,*,#3345,.T.);
#4097=ORIENTED_EDGE('',*,*,#3344,.T.);
#4098=ORIENTED_EDGE('',*,*,#3346,.F.);
#4099=ORIENTED_EDGE('',*,*,#3336,.F.);
#4100=ORIENTED_EDGE('',*,*,#3346,.T.);
#4101=ORIENTED_EDGE('',*,*,#3343,.T.);
#4102=ORIENTED_EDGE('',*,*,#3340,.T.);
#4103=ORIENTED_EDGE('',*,*,#3337,.T.);
#4104=ORIENTED_EDGE('',*,*,#3325,.T.);
#4105=ORIENTED_EDGE('',*,*,#3328,.T.);
#4106=ORIENTED_EDGE('',*,*,#3331,.T.);
#4107=ORIENTED_EDGE('',*,*,#3334,.T.);
#4108=ORIENTED_EDGE('',*,*,#3345,.F.);
#4109=ORIENTED_EDGE('',*,*,#3335,.F.);
#4110=ORIENTED_EDGE('',*,*,#3339,.F.);
#4111=ORIENTED_EDGE('',*,*,#3342,.F.);
#4112=ORIENTED_EDGE('',*,*,#3323,.T.);
#4113=ORIENTED_EDGE('',*,*,#3326,.T.);
#4114=ORIENTED_EDGE('',*,*,#3329,.T.);
#4115=ORIENTED_EDGE('',*,*,#3332,.T.);
#5558=CYLINDRICAL_SURFACE('',#6504,0.21);
#5559=CYLINDRICAL_SURFACE('',#6507,0.21);
#5560=CYLINDRICAL_SURFACE('',#6510,0.21);
#5561=CYLINDRICAL_SURFACE('',#6513,0.21);
#5695=ADVANCED_FACE('',(#796),#5558,.F.);
#5696=ADVANCED_FACE('',(#797),#5559,.F.);
#5697=ADVANCED_FACE('',(#798),#5560,.F.);
#5698=ADVANCED_FACE('',(#799),#5561,.F.);
#5699=ADVANCED_FACE('',(#800),#570,.T.);
#5700=ADVANCED_FACE('',(#801),#571,.T.);
#5701=ADVANCED_FACE('',(#802),#572,.T.);
#5702=ADVANCED_FACE('',(#803),#573,.T.);
#5703=ADVANCED_FACE('',(#804,#402,#403,#404,#405),#574,.T.);
#5704=ADVANCED_FACE('',(#805,#406,#407,#408,#409),#575,.F.);
#6067=CLOSED_SHELL('',(#5695,#5696,#5697,#5698,#5699,#5700,#5701,#5702,
#5703,#5704));
#6503=AXIS2_PLACEMENT_3D('',#9193,#7261,#7262);
#6504=AXIS2_PLACEMENT_3D('',#9194,#7263,#7264);
#6505=AXIS2_PLACEMENT_3D('',#9196,#7265,#7266);
#6506=AXIS2_PLACEMENT_3D('',#9199,#7268,#7269);
#6507=AXIS2_PLACEMENT_3D('',#9200,#7270,#7271);
#6508=AXIS2_PLACEMENT_3D('',#9202,#7272,#7273);
#6509=AXIS2_PLACEMENT_3D('',#9205,#7275,#7276);
#6510=AXIS2_PLACEMENT_3D('',#9206,#7277,#7278);
#6511=AXIS2_PLACEMENT_3D('',#9208,#7279,#7280);
#6512=AXIS2_PLACEMENT_3D('',#9211,#7282,#7283);
#6513=AXIS2_PLACEMENT_3D('',#9212,#7284,#7285);
#6514=AXIS2_PLACEMENT_3D('',#9214,#7286,#7287);
#6515=AXIS2_PLACEMENT_3D('',#9217,#7289,#7290);
#6516=AXIS2_PLACEMENT_3D('',#9218,#7291,#7292);
#6517=AXIS2_PLACEMENT_3D('',#9227,#7297,#7298);
#6518=AXIS2_PLACEMENT_3D('',#9233,#7302,#7303);
#6519=AXIS2_PLACEMENT_3D('',#9239,#7307,#7308);
#6520=AXIS2_PLACEMENT_3D('',#9242,#7311,#7312);
#6521=AXIS2_PLACEMENT_3D('',#9243,#7313,#7314);
#7261=DIRECTION('axis',(0.,0.,1.));
#7262=DIRECTION('refdir',(1.,0.,0.));
#7263=DIRECTION('center_axis',(0.,0.,1.));
#7264=DIRECTION('ref_axis',(1.,0.,0.));
#7265=DIRECTION('center_axis',(0.,0.,1.));
#7266=DIRECTION('ref_axis',(1.,0.,0.));
#7267=DIRECTION('',(0.,0.,1.));
#7268=DIRECTION('center_axis',(0.,0.,-1.));
#7269=DIRECTION('ref_axis',(1.,0.,0.));
#7270=DIRECTION('center_axis',(0.,0.,1.));
#7271=DIRECTION('ref_axis',(1.,0.,0.));
#7272=DIRECTION('center_axis',(0.,0.,1.));
#7273=DIRECTION('ref_axis',(1.,0.,0.));
#7274=DIRECTION('',(0.,0.,1.));
#7275=DIRECTION('center_axis',(0.,0.,-1.));
#7276=DIRECTION('ref_axis',(1.,0.,0.));
#7277=DIRECTION('center_axis',(0.,0.,1.));
#7278=DIRECTION('ref_axis',(1.,0.,0.));
#7279=DIRECTION('center_axis',(0.,0.,1.));
#7280=DIRECTION('ref_axis',(1.,0.,0.));
#7281=DIRECTION('',(0.,0.,1.));
#7282=DIRECTION('center_axis',(0.,0.,-1.));
#7283=DIRECTION('ref_axis',(1.,0.,0.));
#7284=DIRECTION('center_axis',(0.,0.,1.));
#7285=DIRECTION('ref_axis',(1.,0.,0.));
#7286=DIRECTION('center_axis',(0.,0.,1.));
#7287=DIRECTION('ref_axis',(1.,0.,0.));
#7288=DIRECTION('',(0.,0.,1.));
#7289=DIRECTION('center_axis',(0.,0.,-1.));
#7290=DIRECTION('ref_axis',(1.,0.,0.));
#7291=DIRECTION('center_axis',(0.,1.,0.));
#7292=DIRECTION('ref_axis',(-1.,0.,0.));
#7293=DIRECTION('',(-1.,0.,0.));
#7294=DIRECTION('',(0.,0.,1.));
#7295=DIRECTION('',(-1.,0.,0.));
#7296=DIRECTION('',(0.,0.,1.));
#7297=DIRECTION('center_axis',(1.,0.,0.));
#7298=DIRECTION('ref_axis',(0.,1.,0.));
#7299=DIRECTION('',(0.,1.,0.));
#7300=DIRECTION('',(0.,1.,0.));
#7301=DIRECTION('',(0.,0.,1.));
#7302=DIRECTION('center_axis',(0.,-1.,0.));
#7303=DIRECTION('ref_axis',(1.,0.,0.));
#7304=DIRECTION('',(1.,0.,0.));
#7305=DIRECTION('',(1.,0.,0.));
#7306=DIRECTION('',(0.,0.,1.));
#7307=DIRECTION('center_axis',(-1.,0.,0.));
#7308=DIRECTION('ref_axis',(0.,-1.,0.));
#7309=DIRECTION('',(0.,-1.,0.));
#7310=DIRECTION('',(0.,-1.,0.));
#7311=DIRECTION('center_axis',(0.,0.,1.));
#7312=DIRECTION('ref_axis',(1.,0.,0.));
#7313=DIRECTION('center_axis',(0.,0.,1.));
#7314=DIRECTION('ref_axis',(1.,0.,0.));
#9193=CARTESIAN_POINT('',(0.,0.,0.));
#9194=CARTESIAN_POINT('Origin',(4.5,-1.8,-0.1));
#9195=CARTESIAN_POINT('',(4.29,-1.8,0.));
#9196=CARTESIAN_POINT('Origin',(4.5,-1.8,0.));
#9197=CARTESIAN_POINT('',(4.29,-1.8,0.8));
#9198=CARTESIAN_POINT('',(4.29,-1.8,-0.1));
#9199=CARTESIAN_POINT('Origin',(4.5,-1.8,0.8));
#9200=CARTESIAN_POINT('Origin',(-4.5,1.8,-0.1));
#9201=CARTESIAN_POINT('',(-4.71,1.8,0.));
#9202=CARTESIAN_POINT('Origin',(-4.5,1.8,0.));
#9203=CARTESIAN_POINT('',(-4.71,1.8,0.8));
#9204=CARTESIAN_POINT('',(-4.71,1.8,-0.1));
#9205=CARTESIAN_POINT('Origin',(-4.5,1.8,0.8));
#9206=CARTESIAN_POINT('Origin',(-4.5,-1.8,-0.1));
#9207=CARTESIAN_POINT('',(-4.71,-1.8,0.));
#9208=CARTESIAN_POINT('Origin',(-4.5,-1.8,0.));
#9209=CARTESIAN_POINT('',(-4.71,-1.8,0.8));
#9210=CARTESIAN_POINT('',(-4.71,-1.8,-0.1));
#9211=CARTESIAN_POINT('Origin',(-4.5,-1.8,0.8));
#9212=CARTESIAN_POINT('Origin',(4.5,1.8,-0.1));
#9213=CARTESIAN_POINT('',(4.29,1.8,0.));
#9214=CARTESIAN_POINT('Origin',(4.5,1.8,0.));
#9215=CARTESIAN_POINT('',(4.29,1.8,0.8));
#9216=CARTESIAN_POINT('',(4.29,1.8,-0.1));
#9217=CARTESIAN_POINT('Origin',(4.5,1.8,0.8));
#9218=CARTESIAN_POINT('Origin',(7.,3.5,0.));
#9219=CARTESIAN_POINT('',(7.,3.5,0.));
#9220=CARTESIAN_POINT('',(-7.,3.5,0.));
#9221=CARTESIAN_POINT('',(7.,3.5,0.));
#9222=CARTESIAN_POINT('',(-7.,3.5,0.8));
#9223=CARTESIAN_POINT('',(-7.,3.5,0.));
#9224=CARTESIAN_POINT('',(7.,3.5,0.8));
#9225=CARTESIAN_POINT('',(7.,3.5,0.8));
#9226=CARTESIAN_POINT('',(7.,3.5,0.));
#9227=CARTESIAN_POINT('Origin',(7.,-3.5,0.));
#9228=CARTESIAN_POINT('',(7.,-3.5,0.));
#9229=CARTESIAN_POINT('',(7.,-3.5,0.));
#9230=CARTESIAN_POINT('',(7.,-3.5,0.8));
#9231=CARTESIAN_POINT('',(7.,-3.5,0.8));
#9232=CARTESIAN_POINT('',(7.,-3.5,0.));
#9233=CARTESIAN_POINT('Origin',(-7.,-3.5,0.));
#9234=CARTESIAN_POINT('',(-7.,-3.5,0.));
#9235=CARTESIAN_POINT('',(-7.,-3.5,0.));
#9236=CARTESIAN_POINT('',(-7.,-3.5,0.8));
#9237=CARTESIAN_POINT('',(-7.,-3.5,0.8));
#9238=CARTESIAN_POINT('',(-7.,-3.5,0.));
#9239=CARTESIAN_POINT('Origin',(-7.,3.5,0.));
#9240=CARTESIAN_POINT('',(-7.,3.5,0.));
#9241=CARTESIAN_POINT('',(-7.,3.5,0.8));
#9242=CARTESIAN_POINT('Origin',(0.,0.,0.8));
#9243=CARTESIAN_POINT('Origin',(0.,0.,0.));
#11356=UNCERTAINTY_MEASURE_WITH_UNIT(LENGTH_MEASURE(0.001),#11433,
'DISTANCE_ACCURACY_VALUE',
'Maximum model space distance between geometric entities at asserted c
onnectivities');
#11393=UNCERTAINTY_MEASURE_WITH_UNIT(LENGTH_MEASURE(0.001),#11433,
'DISTANCE_ACCURACY_VALUE',
'Maximum model space distance between geometric entities at asserted c
onnectivities');
#11395=(
GEOMETRIC_REPRESENTATION_CONTEXT(3)
GLOBAL_UNCERTAINTY_ASSIGNED_CONTEXT((#11356))
GLOBAL_UNIT_ASSIGNED_CONTEXT((#11433,#11435,#11436))
REPRESENTATION_CONTEXT('','3D')
);
#11432=(
GEOMETRIC_REPRESENTATION_CONTEXT(3)
GLOBAL_UNCERTAINTY_ASSIGNED_CONTEXT((#11393))
GLOBAL_UNIT_ASSIGNED_CONTEXT((#11433,#11435,#11436))
REPRESENTATION_CONTEXT('','3D')
);
#11433=(
LENGTH_UNIT()
NAMED_UNIT(*)
SI_UNIT(.CENTI.,.METRE.)
);
#11435=(
NAMED_UNIT(*)
PLANE_ANGLE_UNIT()
SI_UNIT($,.RADIAN.)
);
#11436=(
NAMED_UNIT(*)
SI_UNIT($,.STERADIAN.)
SOLID_ANGLE_UNIT()
);
#11438=SHAPE_DEFINITION_REPRESENTATION(#11476,#11564);
#11476=PRODUCT_DEFINITION_SHAPE('',$,#11603);
#11564=SHAPE_REPRESENTATION('',(#6503),#11395);
#11601=PRODUCT_DEFINITION_CONTEXT('part definition',#11717,'design');
#11603=PRODUCT_DEFINITION('Base','Base',#11641,#11601);
#11641=PRODUCT_DEFINITION_FORMATION('',$,#11720);
#11717=APPLICATION_CONTEXT(
'Core Data for Automotive Mechanical Design Process');
#11718=PRODUCT_CONTEXT('part definition',#11717,'mechanical');
#11720=PRODUCT('Base','Base','Base',(#11718));
#11792=COLOUR_RGB('Dark Blue',0.08,0.2,0.34);
#11793=FILL_AREA_STYLE_COLOUR('',#11792);
#11794=FILL_AREA_STYLE('',(#11793));
#11795=SURFACE_STYLE_FILL_AREA(#11794);
#11796=SURFACE_SIDE_STYLE('',(#11795));
#11797=SURFACE_STYLE_USAGE(.BOTH.,#11796);
#11798=PRESENTATION_STYLE_ASSIGNMENT((#11797));
ENDSEC;
END-ISO-10303-21;
